ISO-10303-21;
HEADER;
FILE_DESCRIPTION (('STEP AP214'),
    '1' );
FILE_NAME ('Bolt M6.step',
    '2026-10-06T09:00:30',
    ( '' ),
    ( '' ),
    'SwSTEP 2.0',
    'SolidWorks 2020',
    '' );
FILE_SCHEMA (( 'AUTOMOTIVE_DESIGN' ));
ENDSEC;

DATA;
#4=EDGE_CURVE ( 'NONE', #19777, #16714, #24382, .T. ) ;
#5=EDGE_CURVE ( 'NONE', #10372, #13996, #4280, .T. ) ;
#46=AXIS2_PLACEMENT_3D ( 'NONE', #29369, #26557, #19627 ) ;
#54=PRODUCT_DEFINITION ( 'UNKNOWN', '', #25430, #25414 ) ;
#57=EDGE_LOOP ( 'NONE', ( #4561, #8496, #21991, #5977, #22039 ) ) ;
#64=EDGE_CURVE ( 'NONE', #9917, #25371, #9300, .T. ) ;
#163=ORIENTED_EDGE ( 'NONE', *, *, #204, .F. ) ;
#204=EDGE_CURVE ( 'NONE', #15790, #12797, #14647, .T. ) ;
#211=CARTESIAN_POINT ( 'NONE',  ( -19.29999999990000248, -25.07317073083999759, -28.39999999989999324 ) ) ;
#242=AXIS2_PLACEMENT_3D ( 'NONE', #1141, #8056, #25215 ) ;
#355=CARTESIAN_POINT ( 'NONE',  ( 12.80098767942999771, -22.00000000000000000, -31.28675134584999640 ) ) ;
#358=DIRECTION ( 'NONE',  ( 1.000000000000000000, 0.000000000000000000, 0.000000000000000000 ) ) ;
#384=AXIS2_PLACEMENT_3D ( 'NONE', #23871, #9212, #21346 ) ;
#437=EDGE_CURVE ( 'NONE', #12797, #28640, #22954, .T. ) ;
#610=CARTESIAN_POINT ( 'NONE',  ( 14.40197535836999876, -27.00000000000014566, -22.62649730800000114 ) ) ;
#626=FACE_BOUND ( 'NONE', #15131, .T. ) ;
#673=EDGE_CURVE ( 'NONE', #7295, #15790, #18185, .T. ) ;
#686=ORIENTED_EDGE ( 'NONE', *, *, #13583, .T. ) ;
#737=DIRECTION ( 'NONE',  ( 0.000000000000000000, -0.9624904629342537765, 0.2713155151490711514 ) ) ;
#766=CARTESIAN_POINT ( 'NONE',  ( 11.20000000009999930, -22.00000000000000000, -31.28675134584999640 ) ) ;
#782=EDGE_CURVE ( 'NONE', #19357, #7295, #2457, .T. ) ;
#844=DIRECTION ( 'NONE',  ( 1.000000000000000000, 0.000000000000000000, 0.000000000000000000 ) ) ;
#874=CARTESIAN_POINT ( 'NONE',  ( 11.20000000009999930, -27.00000000000000355, -22.62649730800000114 ) ) ;
#897=CARTESIAN_POINT ( 'NONE',  ( 14.40197535836999876, -22.00000000000000000, -31.28675134584999640 ) ) ;
#1050=EDGE_CURVE ( 'NONE', #7923, #29336, #21124, .T. ) ;
#1100=CARTESIAN_POINT ( 'NONE',  ( -20.22682926819999949, -27.00000000000000000, -28.39999999989999679 ) ) ;
#1101=EDGE_CURVE ( 'NONE', #7295, #11539, #25974, .T. ) ;
#1112=ORIENTED_EDGE ( 'NONE', *, *, #24670, .T. ) ;
#1141=CARTESIAN_POINT ( 'NONE',  ( -18.29999999989999893, -27.00000000000000000, -28.39999999989999679 ) ) ;
#1172=AXIS2_PLACEMENT_3D ( 'NONE', #21552, #13688, #21400 ) ;
#1201=CARTESIAN_POINT ( 'NONE',  ( 14.72975346149532960, -25.75642680092629888, -33.45521746712941535 ) ) ;
#1257=AXIS2_PLACEMENT_3D ( 'NONE', #22632, #24529, #15386 ) ;
#1351=EDGE_CURVE ( 'NONE', #5093, #30733, #10522, .T. ) ;
#1354=VECTOR ( 'NONE', #6354, 1000.000000000000000 ) ;
#1358=FACE_OUTER_BOUND ( 'NONE', #16961, .T. ) ;
#1365=ADVANCED_FACE ( 'NONE', ( #1358 ), #15662, .T. ) ;
#1387=FACE_OUTER_BOUND ( 'NONE', #57, .T. ) ;
#1451=VECTOR ( 'NONE', #7899, 1000.000000000000114 ) ;
#1536=VERTEX_POINT ( 'NONE', #26055 ) ;
#1574=CARTESIAN_POINT ( 'NONE',  ( 11.20000000009999930, -27.00000000000000355, -22.62649730800000114 ) ) ;
#1635=VERTEX_POINT ( 'NONE', #20464 ) ;
#1717=CARTESIAN_POINT ( 'NONE',  ( 14.83997978847363619, -29.88586221491316053, -24.29280345199157054 ) ) ;
#1736=AXIS2_PLACEMENT_3D ( 'NONE', #9220, #16004, #14272 ) ;
#1792=ORIENTED_EDGE ( 'NONE', *, *, #3920, .T. ) ;
#1851=DIRECTION ( 'NONE',  ( 1.000000000000000000, 0.000000000000000000, 0.000000000000000000 ) ) ;
#1862=ORIENTED_EDGE ( 'NONE', *, *, #1050, .F. ) ;
#1944=EDGE_LOOP ( 'NONE', ( #7584, #29136, #1792, #3087 ) ) ;
#1983=AXIS2_PLACEMENT_3D ( 'NONE', #20686, #8871, #4163 ) ;
#1987=FILL_AREA_STYLE ('',( #18340 ) ) ;
#2004=CARTESIAN_POINT ( 'NONE',  ( 14.47923079777836008, -32.00000000000144951, -25.78086934637092753 ) ) ;
#2024=EDGE_LOOP ( 'NONE', ( #11963, #29832 ) ) ;
#2075=ORIENTED_EDGE ( 'NONE', *, *, #1351, .F. ) ;
#2136=( NAMED_UNIT ( * ) PLANE_ANGLE_UNIT ( ) SI_UNIT ( $, .RADIAN. ) );
#2181=CARTESIAN_POINT ( 'NONE',  ( 14.63279312439116531, -27.79071840260195003, -23.08346332393403699 ) ) ;
#2221=CARTESIAN_POINT ( 'NONE',  ( 11.20000000009999930, -32.00000000000000000, -31.28675134584999640 ) ) ;
#2273=DIRECTION ( 'NONE',  ( 1.000000000000000000, 0.000000000000000000, 0.000000000000000000 ) ) ;
#2298=DIRECTION ( 'NONE',  ( 0.000000000000000000, -1.000000000000000000, 0.000000000000000000 ) ) ;
#2304=CARTESIAN_POINT ( 'NONE',  ( -4.299999999899999814, -27.00000000000000000, -28.39999999989999679 ) ) ;
#2387=EDGE_LOOP ( 'NONE', ( #6499, #20813, #11864, #16053 ) ) ;
#2457=LINE ( 'NONE', #31092, #18574 ) ;
#2554=VERTEX_POINT ( 'NONE', #9874 ) ;
#2583=EDGE_CURVE ( 'NONE', #2554, #19777, #7060, .T. ) ;
#2627=CARTESIAN_POINT ( 'NONE',  ( 0.000000000000000000, 0.000000000000000000, 0.000000000000000000 ) ) ;
#2666=ORIENTED_EDGE ( 'NONE', *, *, #22345, .T. ) ;
#2677=DIRECTION ( 'NONE',  ( 1.000000000000000000, 0.000000000000000000, 0.000000000000000000 ) ) ;
#2692=CARTESIAN_POINT ( 'NONE',  ( 11.20000000009999930, -21.99999999940999729, -31.28675134550999815 ) ) ;
#2696=TOROIDAL_SURFACE ( 'NONE', #29324, 3.176829268290000563, 0.2500000000000000000 ) ;
#2699=DIRECTION ( 'NONE',  ( 0.000000000000000000, 0.9624904629342537765, -0.2713155151490711514 ) ) ;
#2774=AXIS2_PLACEMENT_3D ( 'NONE', #27249, #27402, #20472 ) ;
#2803=DIRECTION ( 'NONE',  ( 1.000000000000000000, 0.000000000000000000, 0.000000000000000000 ) ) ;
#2844=CARTESIAN_POINT ( 'NONE',  ( -20.22682926819999949, -26.99999999999973355, -28.39999999990017798 ) ) ;
#2852=LINE ( 'NONE', #24418, #13785 ) ;
#2893=AXIS2_PLACEMENT_3D ( 'NONE', #22500, #9248, #18857 ) ;
#2959=DIRECTION ( 'NONE',  ( 0.000000000000000000, -1.000000000000000000, 0.000000000000000000 ) ) ;
#2974=DIRECTION ( 'NONE',  ( -1.000000000000000000, 0.000000000000000000, 0.000000000000000000 ) ) ;
#3004=LINE ( 'NONE', #355, #22263 ) ;
#3087=ORIENTED_EDGE ( 'NONE', *, *, #6006, .T. ) ;
#3129=EDGE_CURVE ( 'NONE', #4371, #5093, #26335, .T. ) ;
#3170=CARTESIAN_POINT ( 'NONE',  ( 10.70000000009999930, -27.00000000000000000, -28.39999999989999679 ) ) ;
#3219=CARTESIAN_POINT ( 'NONE',  ( 14.77468706462038561, -31.99974765295981882, -29.54175819371382872 ) ) ;
#3235=COLOUR_RGB ( '', 0.72549020, 0.75294118, 0.79215686) ;
#3276=ORIENTED_EDGE ( 'NONE', *, *, #29739, .F. ) ;
#3289=PLANE ( 'NONE',  #2893 ) ;
#3312=ORIENTED_EDGE ( 'NONE', *, *, #9351, .T. ) ;
#3368=CARTESIAN_POINT ( 'NONE',  ( 14.40197535836999876, -32.00000000000000000, -31.28675134584999640 ) ) ;
#3371=CARTESIAN_POINT ( 'NONE',  ( 14.78499923084528866, -31.99972756340226709, -29.45768886394915143 ) ) ;
#3389=CARTESIAN_POINT ( 'NONE',  ( 14.67158610511051364, -22.90305194238077036, -31.80764456536135043 ) ) ;
#3419=DIRECTION ( 'NONE',  ( 0.000000000000000000, -1.000000000000000000, 0.000000000000000000 ) ) ;
#3439=LINE ( 'NONE', #3763, #23515 ) ;
#3611=DIRECTION ( 'NONE',  ( -1.000000000000000000, 0.000000000000000000, 0.000000000000000000 ) ) ;
#3663=ORIENTED_EDGE ( 'NONE', *, *, #21563, .F. ) ;
#3739=CARTESIAN_POINT ( 'NONE',  ( 14.84775334008999970, -24.60220466919999893, -24.01086508770000094 ) ) ;
#3743=TOROIDAL_SURFACE ( 'NONE', #17786, 3.176829268290000563, 0.2500000000000000000 ) ;
#3763=CARTESIAN_POINT ( 'NONE',  ( 11.20000000009999930, -32.00000000000000000, -28.39999999989999679 ) ) ;
#3836=ORIENTED_EDGE ( 'NONE', *, *, #3920, .F. ) ;
#3868=( LENGTH_UNIT ( ) NAMED_UNIT ( * ) SI_UNIT ( .MILLI., .METRE. ) );
#3875=EDGE_CURVE ( 'NONE', #25571, #9871, #3439, .T. ) ;
#3900=CARTESIAN_POINT ( 'NONE',  ( 14.84171152945961047, -24.10535842370141424, -24.29771940128471996 ) ) ;
#3915=CARTESIAN_POINT ( 'NONE',  ( 14.75521759265642707, -30.61078560332397913, -24.71147133353610315 ) ) ;
#3920=EDGE_CURVE ( 'NONE', #6451, #1635, #13513, .T. ) ;
#3959=CARTESIAN_POINT ( 'NONE',  ( 14.67495062122367599, -22.00000000000000000, -26.63047724528842153 ) ) ;
#3962=ORIENTED_EDGE ( 'NONE', *, *, #7255, .F. ) ;
#3996=ADVANCED_FACE ( 'NONE', ( #27213, #15251 ), #3289, .F. ) ;
#4019=SURFACE_SIDE_STYLE ('',( #21015 ) ) ;
#4026=CARTESIAN_POINT ( 'NONE',  ( 14.74927456580481966, -23.35383567438356778, -32.06809451559220747 ) ) ;
#4057=CARTESIAN_POINT ( 'NONE',  ( 14.76039189739984359, -23.42146364767391375, -24.69256623432178088 ) ) ;
#4090=PLANE ( 'NONE',  #1172 ) ;
#4103=VERTEX_POINT ( 'NONE', #6889 ) ;
#4113=CARTESIAN_POINT ( 'NONE',  ( 14.75185518689595376, -21.99999999999999645, -29.70934853584909874 ) ) ;
#4163=DIRECTION ( 'NONE',  ( 0.000000000000000000, 1.000000000000000000, 0.000000000000000000 ) ) ;
#4170=DIRECTION ( 'NONE',  ( 1.000000000000000000, 0.000000000000000000, 0.000000000000000000 ) ) ;
#4185=LINE ( 'NONE', #16451, #15928 ) ;
#4189=DIRECTION ( 'NONE',  ( 0.000000000000000000, -0.8660254037843289066, 0.5000000000001899592 ) ) ;
#4210=CARTESIAN_POINT ( 'NONE',  ( 14.84775334008999970, -29.39779533080000107, -32.78913491209999620 ) ) ;
#4225=VECTOR ( 'NONE', #2677, 1000.000000000000000 ) ;
#4228=CARTESIAN_POINT ( 'NONE',  ( 14.40197535836999876, -32.00000000000000000, -25.51324865394999719 ) ) ;
#4229=CARTESIAN_POINT ( 'NONE',  ( -19.29999999990000248, -27.00000000000000000, -28.39999999989999679 ) ) ;
#4256=ORIENTED_EDGE ( 'NONE', *, *, #18238, .F. ) ;
#4280=CIRCLE ( 'NONE', #20353, 2.926829268290000119 ) ;
#4371=VERTEX_POINT ( 'NONE', #26069 ) ;
#4380=CARTESIAN_POINT ( 'NONE',  ( 14.40197535836999876, -27.00000000000014566, -22.62649730800000114 ) ) ;
#4388=CARTESIAN_POINT ( 'NONE',  ( 11.20000000009999930, -32.00000000000000000, -31.28675134584999640 ) ) ;
#4432=VECTOR ( 'NONE', #12645, 1000.000000000000227 ) ;
#4494=( LENGTH_UNIT ( ) NAMED_UNIT ( * ) SI_UNIT ( .MILLI., .METRE. ) );
#4561=ORIENTED_EDGE ( 'NONE', *, *, #26132, .F. ) ;
#4564=CARTESIAN_POINT ( 'NONE',  ( 14.47923079777919142, -26.76823368177736739, -34.03969234558647372 ) ) ;
#4685=ORIENTED_EDGE ( 'NONE', *, *, #7721, .T. ) ;
#4742=VECTOR ( 'NONE', #12840, 1000.000000000000114 ) ;
#4743=EDGE_LOOP ( 'NONE', ( #7044, #3276, #18654, #13099, #12888, #22337, #17132 ) ) ;
#4762=PLANE ( 'NONE',  #15787 ) ;
#4770=ORIENTED_EDGE ( 'NONE', *, *, #5, .F. ) ;
#4819=CARTESIAN_POINT ( 'NONE',  ( -4.299999999899999814, -24.07317073171000033, -28.39999999989999679 ) ) ;
#4849=ORIENTED_EDGE ( 'NONE', *, *, #18735, .F. ) ;
#4908=DIRECTION ( 'NONE',  ( 0.7071067811870476172, -0.7071067811860475283, 1.007806864420067330E-13 ) ) ;
#4909=ORIENTED_EDGE ( 'NONE', *, *, #29739, .T. ) ;
#4982=AXIS2_PLACEMENT_3D ( 'NONE', #874, #12660, #8236 ) ;
#5056=CARTESIAN_POINT ( 'NONE',  ( 14.80325893430790707, -25.27741815202685416, -23.62134642851259869 ) ) ;
#5093=VERTEX_POINT ( 'NONE', #30564 ) ;
#5117=CARTESIAN_POINT ( 'NONE',  ( 14.81448010921107539, -31.99990471976291317, -27.51316145670302404 ) ) ;
#5188=LINE ( 'NONE', #19055, #14946 ) ;
#5204=DIRECTION ( 'NONE',  ( 1.000000000000000000, 0.000000000000000000, 0.000000000000000000 ) ) ;
#5255=CIRCLE ( 'NONE', #13288, 2.926829268290000119 ) ;
#5285=CARTESIAN_POINT ( 'NONE',  ( 14.74927456580200946, -31.99974519688053576, -29.72362367442748976 ) ) ;
#5290=DIRECTION ( 'NONE',  ( 0.000000000000000000, 1.665334536939999828E-16, -1.000000000000000000 ) ) ;
#5293=CARTESIAN_POINT ( 'NONE',  ( 10.45000000009999930, -26.99999999999950617, -28.39999999990030588 ) ) ;
#5429=CARTESIAN_POINT ( 'NONE',  ( 14.74466352504733813, -31.99976755572771836, -27.04560447322398176 ) ) ;
#5467=CIRCLE ( 'NONE', #1983, 4.439999999999999503 ) ;
#5520=LINE ( 'NONE', #20615, #22300 ) ;
#5548=EDGE_CURVE ( 'NONE', #9016, #24581, #10295, .T. ) ;
#5592=EDGE_CURVE ( 'NONE', #19446, #4103, #29366, .T. ) ;
#5623=DIRECTION ( 'NONE',  ( -1.000000000000000000, 0.000000000000000000, 0.000000000000000000 ) ) ;
#5648=FACE_OUTER_BOUND ( 'NONE', #21683, .T. ) ;
#5677=CIRCLE ( 'NONE', #20755, 2.926829268290000119 ) ;
#5737=CARTESIAN_POINT ( 'NONE',  ( 14.55660443455950315, -32.00000000000113687, -30.75110051328497462 ) ) ;
#5739=STYLED_ITEM ( 'NONE', ( #30462 ), #21644 ) ;
#5861=EDGE_LOOP ( 'NONE', ( #18459, #27736, #10262, #9953 ) ) ;
#5905=CARTESIAN_POINT ( 'NONE',  ( 14.78499923084739720, -23.58415079274018566, -32.20104664978513398 ) ) ;
#5948=ORIENTED_EDGE ( 'NONE', *, *, #8522, .T. ) ;
#5968=EDGE_CURVE ( 'NONE', #25254, #9917, #22841, .T. ) ;
#5977=ORIENTED_EDGE ( 'NONE', *, *, #7255, .T. ) ;
#6006=EDGE_CURVE ( 'NONE', #1635, #10372, #13792, .T. ) ;
#6042=PRODUCT ( 'Bolt M6', 'Bolt M6', '', ( #10996 ) ) ;
#6066=CARTESIAN_POINT ( 'NONE',  ( 14.84842474946499280, -24.30580232298240517, -32.61831005400841121 ) ) ;
#6150=CARTESIAN_POINT ( 'NONE',  ( -18.29999999989999893, -27.00000000000000000, -28.39999999989999679 ) ) ;
#6354=DIRECTION ( 'NONE',  ( 1.000000000000000000, 0.000000000000000000, 0.000000000000000000 ) ) ;
#6415=CARTESIAN_POINT ( 'NONE',  ( 14.40197535836999876, -26.99999999999984368, -34.17350269180000311 ) ) ;
#6416=DIRECTION ( 'NONE',  ( 0.000000000000000000, -1.000000000000000000, 0.000000000000000000 ) ) ;
#6420=EDGE_LOOP ( 'NONE', ( #24916, #18299, #5948 ) ) ;
#6451=VERTEX_POINT ( 'NONE', #211 ) ;
#6499=ORIENTED_EDGE ( 'NONE', *, *, #17874, .F. ) ;
#6526=CLOSED_SHELL ( 'NONE', ( #18054, #16934, #28376, #11467, #18348, #10191, #23767, #24652, #26952, #25198, #12769, #11206, #30071, #13435, #3996, #7098, #8104, #19469, #29345, #1365, #14132, #29016 ) ) ;
#6547=CARTESIAN_POINT ( 'NONE',  ( 10.45000000009999930, -23.82317073171000033, -28.39999999989999679 ) ) ;
#6581=CARTESIAN_POINT ( 'NONE',  ( 14.80403571755123870, -30.27061049443689456, -24.51513120827885217 ) ) ;
#6582=DIRECTION ( 'NONE',  ( -1.000000000000000000, 1.646361269960000031E-16, 1.110223024630000146E-15 ) ) ;
#6600=FACE_OUTER_BOUND ( 'NONE', #6420, .T. ) ;
#6638=FACE_OUTER_BOUND ( 'NONE', #4743, .T. ) ;
#6695=FACE_OUTER_BOUND ( 'NONE', #19854, .T. ) ;
#6746=ORIENTED_EDGE ( 'NONE', *, *, #10073, .F. ) ;
#6834=CARTESIAN_POINT ( 'NONE',  ( 11.20000000009999930, -27.00000000000000000, -28.39999999989999679 ) ) ;
#6889=CARTESIAN_POINT ( 'NONE',  ( 14.85000000009999788, -24.60407027184000128, -24.01428005041999825 ) ) ;
#6971=ORIENTED_EDGE ( 'NONE', *, *, #437, .T. ) ;
#7014=CIRCLE ( 'NONE', #26602, 0.2500000000000002220 ) ;
#7044=ORIENTED_EDGE ( 'NONE', *, *, #7866, .F. ) ;
#7060=CIRCLE ( 'NONE', #46, 2.926829268290000119 ) ;
#7095=DIRECTION ( 'NONE',  ( 1.000000000000000000, 0.000000000000000000, 0.000000000000000000 ) ) ;
#7098=ADVANCED_FACE ( 'NONE', ( #5648 ), #19829, .T. ) ;
#7173=UNCERTAINTY_MEASURE_WITH_UNIT (LENGTH_MEASURE( 1.000000000000000082E-05 ), #3868, 'distance_accuracy_value', 'NONE');
#7255=EDGE_CURVE ( 'NONE', #2554, #1635, #26215, .T. ) ;
#7295=VERTEX_POINT ( 'NONE', #17378 ) ;
#7300=ORIENTED_EDGE ( 'NONE', *, *, #5592, .T. ) ;
#7374=PLANE ( 'NONE',  #22565 ) ;
#7442=DIRECTION ( 'NONE',  ( 0.000000000000000000, 0.2713155151490714290, 0.9624904629342537765 ) ) ;
#7546=AXIS2_PLACEMENT_3D ( 'NONE', #23981, #2273, #31057 ) ;
#7584=ORIENTED_EDGE ( 'NONE', *, *, #13774, .F. ) ;
#7631=CARTESIAN_POINT ( 'NONE',  ( 14.65905325912865997, -31.99961021129703909, -26.55383800025211372 ) ) ;
#7642=LINE ( 'NONE', #10331, #4742 ) ;
#7720=ORIENTED_EDGE ( 'NONE', *, *, #25675, .F. ) ;
#7721=EDGE_CURVE ( 'NONE', #25371, #19777, #7014, .T. ) ;
#7742=DIRECTION ( 'NONE',  ( 1.000000000000000000, 0.000000000000000000, 0.000000000000000000 ) ) ;
#7764=CONICAL_SURFACE ( 'NONE', #10780, 0.9999999999991012745, 0.7853981633970000820 ) ;
#7786=CARTESIAN_POINT ( 'NONE',  ( 14.84835410051233850, -32.00028618471380071, -27.94962782489255915 ) ) ;
#7822=ORIENTED_EDGE ( 'NONE', *, *, #782, .F. ) ;
#7864=CARTESIAN_POINT ( 'NONE',  ( 14.85000000009999788, -29.39592972815999872, -32.78571994937999534 ) ) ;
#7866=EDGE_CURVE ( 'NONE', #11539, #30733, #12750, .T. ) ;
#7868=CARTESIAN_POINT ( 'NONE',  ( 14.76223730231795273, -25.56820193551933329, -23.45324323474691042 ) ) ;
#7899=DIRECTION ( 'NONE',  ( 0.7071067811868757547, -0.6804000508938797820, -0.1924987551729659130 ) ) ;
#7923=VERTEX_POINT ( 'NONE', #30232 ) ;
#7937=CARTESIAN_POINT ( 'NONE',  ( 14.83997978847352783, -31.99986765628636576, -28.84563171583047492 ) ) ;
#7956=EDGE_CURVE ( 'NONE', #9016, #7923, #5188, .T. ) ;
#8056=DIRECTION ( 'NONE',  ( -1.000000000000000000, 0.000000000000000000, 0.000000000000000000 ) ) ;
#8076=CARTESIAN_POINT ( 'NONE',  ( -18.29999999989999893, -29.81628579456999972, -29.19678346420899828 ) ) ;
#8087=CARTESIAN_POINT ( 'NONE',  ( 14.84775334008999970, -29.39779533080000107, -32.78913491209999620 ) ) ;
#8104=ADVANCED_FACE ( 'NONE', ( #25951 ), #27830, .T. ) ;
#8128=CARTESIAN_POINT ( 'NONE',  ( 10.45000000009999930, -29.81704525737000111, -27.60590580922099946 ) ) ;
#8223=LINE ( 'NONE', #26974, #4432 ) ;
#8236=DIRECTION ( 'NONE',  ( -1.000000000000000000, 0.000000000000000000, 0.000000000000000000 ) ) ;
#8243=AXIS2_PLACEMENT_3D ( 'NONE', #21352, #30492, #30792 ) ;
#8288=DIRECTION ( 'NONE',  ( 0.000000000000000000, 1.000000000000000000, 0.000000000000000000 ) ) ;
#8344=DIRECTION ( 'NONE',  ( 0.000000000000000000, 1.000000000000000000, 0.000000000000000000 ) ) ;
#8388=ORIENTED_EDGE ( 'NONE', *, *, #5592, .F. ) ;
#8413=CARTESIAN_POINT ( 'NONE',  ( 14.76126683900010761, -23.42592653034165195, -32.10972855315200292 ) ) ;
#8496=ORIENTED_EDGE ( 'NONE', *, *, #4, .F. ) ;
#8522=EDGE_CURVE ( 'NONE', #23742, #12454, #22493, .T. ) ;
#8545=APPLICATION_CONTEXT ( 'automotive_design' ) ;
#8603=CARTESIAN_POINT ( 'NONE',  ( 14.74121624851424528, -28.30819945631988332, -33.41822227976423676 ) ) ;
#8619=CARTESIAN_POINT ( 'NONE',  ( 14.74927456580506835, -30.64616432563845549, -24.73190548423032453 ) ) ;
#8633=DIRECTION ( 'NONE',  ( 0.000000000000000000, 1.000000000000000000, 0.000000000000000000 ) ) ;
#8824=CARTESIAN_POINT ( 'NONE',  ( 14.79876163761986341, -22.00000000000000000, -29.34531477793196785 ) ) ;
#8838=CARTESIAN_POINT ( 'NONE',  ( 10.70000000009999930, -31.44000000000000128, -28.39999999989999679 ) ) ;
#8854=ORIENTED_EDGE ( 'NONE', *, *, #29145, .T. ) ;
#8871=DIRECTION ( 'NONE',  ( 1.000000000000000000, 0.000000000000000000, 0.000000000000000000 ) ) ;
#8924=CARTESIAN_POINT ( 'NONE',  ( 14.76418395427317343, -23.44536579588614700, -24.67876632261722136 ) ) ;
#8925=CARTESIAN_POINT ( 'NONE',  ( 14.76504187223401487, -28.44906468419981138, -33.33684912348113727 ) ) ;
#8975=AXIS2_PLACEMENT_3D ( 'NONE', #6547, #23407, #30317 ) ;
#8985=CARTESIAN_POINT ( 'NONE',  ( 14.83544356365203498, -22.00000000000000355, -28.95333575274569426 ) ) ;
#8989=ORIENTED_EDGE ( 'NONE', *, *, #21563, .T. ) ;
#9014=ORIENTED_EDGE ( 'NONE', *, *, #4, .T. ) ;
#9016=VERTEX_POINT ( 'NONE', #9200 ) ;
#9060=DIRECTION ( 'NONE',  ( -1.000000000000000000, 0.000000000000000000, 0.000000000000000000 ) ) ;
#9080=CIRCLE ( 'NONE', #23176, 3.176829269159998859 ) ;
#9092=CARTESIAN_POINT ( 'NONE',  ( 14.71164558017502699, -28.14786721053526009, -23.28957834311704289 ) ) ;
#9112=B_SPLINE_CURVE_WITH_KNOTS ( 'NONE', 3,
 ( #8087, #15808, #27294, #25419, #13123, #15491, #22895, #25252, #15179, #22731, #3368 ),
 .UNSPECIFIED., .F., .F.,
 ( 4, 1, 1, 1, 2, 2, 4 ),
 ( 0.000000000000000000, 0.2500000000000045519, 0.3750000000000033862, 0.4374999999999993894, 0.4687499999999993339, 0.4999999999999992228, 1.000000000000000000 ),
 .UNSPECIFIED. ) ;
#9134=CARTESIAN_POINT ( 'NONE',  ( 14.67576675165364719, -22.00000000000000000, -30.22138740828507508 ) ) ;
#9165=EDGE_LOOP ( 'NONE', ( #4849, #8388 ) ) ;
#9200=CARTESIAN_POINT ( 'NONE',  ( 10.70000000009999930, -22.55999999999999872, -28.39999999989999679 ) ) ;
#9212=DIRECTION ( 'NONE',  ( -1.000000000000000000, 1.380859481889999837E-13, -9.437625531729999712E-14 ) ) ;
#9220=CARTESIAN_POINT ( 'NONE',  ( 14.85000000009999788, -27.00000000000000000, -28.39999999989999679 ) ) ;
#9241=ORIENTED_EDGE ( 'NONE', *, *, #1101, .F. ) ;
#9248=DIRECTION ( 'NONE',  ( 1.000000000000000000, 0.000000000000000000, 0.000000000000000000 ) ) ;
#9295=CARTESIAN_POINT ( 'NONE',  ( 14.40197535836999876, -22.00000000000000000, -31.28675134584999640 ) ) ;
#9300=CIRCLE ( 'NONE', #10810, 3.176829269159998859 ) ;
#9351=EDGE_CURVE ( 'NONE', #15990, #19446, #8223, .T. ) ;
#9379=APPLICATION_CONTEXT ( 'automotive_design' ) ;
#9452=DIRECTION ( 'NONE',  ( 1.000000000000000000, 0.000000000000000000, 0.000000000000000000 ) ) ;
#9474=DIRECTION ( 'NONE',  ( 0.000000000000000000, -1.000000000000000000, 0.000000000000000000 ) ) ;
#9476=ORIENTED_EDGE ( 'NONE', *, *, #19917, .F. ) ;
#9528=DIRECTION ( 'NONE',  ( 0.000000000000000000, 1.000000000000000000, 0.000000000000000000 ) ) ;
#9602=CARTESIAN_POINT ( 'NONE',  ( 10.70000000009999930, -23.82317073084000114, -28.39999999989999324 ) ) ;
#9625=ORIENTED_EDGE ( 'NONE', *, *, #13427, .F. ) ;
#9664=AXIS2_PLACEMENT_3D ( 'NONE', #1100, #27378, #8633 ) ;
#9848=CARTESIAN_POINT ( 'NONE',  ( 14.84842474946407620, -32.00026250641055015, -28.62408860391630583 ) ) ;
#9871=VERTEX_POINT ( 'NONE', #2221 ) ;
#9873=EDGE_LOOP ( 'NONE', ( #26169, #22381, #30435, #17975, #24972 ) ) ;
#9874=CARTESIAN_POINT ( 'NONE',  ( 10.45000000009999930, -24.07317073171000033, -28.39999999989999679 ) ) ;
#9884=FACE_OUTER_BOUND ( 'NONE', #24572, .T. ) ;
#9917=VERTEX_POINT ( 'NONE', #9602 ) ;
#9953=ORIENTED_EDGE ( 'NONE', *, *, #8522, .F. ) ;
#9982=DIRECTION ( 'NONE',  ( -1.000000000000000000, 1.380859481889999837E-13, -9.437625531729999712E-14 ) ) ;
#10073=EDGE_CURVE ( 'NONE', #1536, #4103, #4185, .T. ) ;
#10160=CARTESIAN_POINT ( 'NONE',  ( 14.69473318574048015, -31.99965463203811211, -26.74399720207908260 ) ) ;
#10165=DIRECTION ( 'NONE',  ( 1.000000000000000000, 0.000000000000000000, 0.000000000000000000 ) ) ;
#10167=CARTESIAN_POINT ( 'NONE',  ( 14.40197535836999876, -32.00000000000000000, -25.51324865394999719 ) ) ;
#10191=ADVANCED_FACE ( 'NONE', ( #6695 ), #30775, .T. ) ;
#10262=ORIENTED_EDGE ( 'NONE', *, *, #24670, .F. ) ;
#10295=CIRCLE ( 'NONE', #8243, 4.439999999999999503 ) ;
#10319=CARTESIAN_POINT ( 'NONE',  ( 14.40197535836999876, -32.00000000000000000, -31.28675134584999640 ) ) ;
#10331=CARTESIAN_POINT ( 'NONE',  ( 11.20000000009999930, -29.50000000000000000, -24.06987298045999779 ) ) ;
#10340=EDGE_LOOP ( 'NONE', ( #12282, #16269, #30055, #3663, #18140, #7822 ) ) ;
#10372=VERTEX_POINT ( 'NONE', #8076 ) ;
#10425=EDGE_CURVE ( 'NONE', #9871, #12600, #28529, .T. ) ;
#10433=LINE ( 'NONE', #15605, #1451 ) ;
#10465=CIRCLE ( 'NONE', #28046, 1.926829268289999231 ) ;
#10521=VECTOR ( 'NONE', #28832, 1000.000000000000000 ) ;
#10522=B_SPLINE_CURVE_WITH_KNOTS ( 'NONE', 3,
 ( #28477, #4564, #23772, #18012, #24958, #15507, #25593, #1201, #25438, #17856, #22751, #27619, #29979, #6066, #10795, #20392, #29678, #5905, #22916, #8413, #15982, #13624, #4026, #3389, #20706, #897 ),
 .UNSPECIFIED., .F., .F.,
 ( 4, 2, 2, 1, 1, 2, 2, 2, 2, 2, 1, 1, 2, 2, 4 ),
 ( 0.000000000000000000, 0.1250000000000019984, 0.1875000000000023870, 0.2187500000000025813, 0.2343750000000010547, 0.2421875000000009992, 0.2500000000000009437, 0.4999999999999972244, 0.6249999999999953371, 0.6874999999999943379, 0.7187499999999937828, 0.7343749999999954481, 0.7421874999999953371, 0.7499999999999952260, 1.000000000000000000 ),
 .UNSPECIFIED. ) ;
#10538=VECTOR ( 'NONE', #4189, 1000.000000000000114 ) ;
#10706=ORIENTED_EDGE ( 'NONE', *, *, #12169, .T. ) ;
#10780=AXIS2_PLACEMENT_3D ( 'NONE', #2844, #24563, #14660 ) ;
#10795=CARTESIAN_POINT ( 'NONE',  ( 14.83997978847463450, -24.11413778510890893, -32.50719654782172796 ) ) ;
#10810=AXIS2_PLACEMENT_3D ( 'NONE', #3170, #20013, #8344 ) ;
#10833=PLANE ( 'NONE',  #1257 ) ;
#10996=PRODUCT_CONTEXT ( 'NONE', #8545, 'mechanical' ) ;
#11012=CIRCLE ( 'NONE', #28603, 0.2500000000000002220 ) ;
#11139=CARTESIAN_POINT ( 'NONE',  ( 14.40197535836999876, -22.00000000000000000, -25.51324865394999719 ) ) ;
#11166=CARTESIAN_POINT ( 'NONE',  ( 11.20000000009999930, -29.49999999969999820, -32.73012701900000110 ) ) ;
#11194=CARTESIAN_POINT ( 'NONE',  ( 14.71344982770164300, -22.00000000000000000, -26.84691114990011584 ) ) ;
#11206=ADVANCED_FACE ( 'NONE', ( #27630 ), #28259, .T. ) ;
#11219=ORIENTED_EDGE ( 'NONE', *, *, #3875, .T. ) ;
#11255=VECTOR ( 'NONE', #18411, 1000.000000000000114 ) ;
#11298=CARTESIAN_POINT ( 'NONE',  ( 14.84482701754090606, -29.21177333770954476, -32.89653475988580311 ) ) ;
#11299=DIRECTION ( 'NONE',  ( -1.000000000000000000, 0.000000000000000000, 0.000000000000000000 ) ) ;
#11308=EDGE_LOOP ( 'NONE', ( #23966, #10706, #20996, #15937 ) ) ;
#11314=CARTESIAN_POINT ( 'NONE',  ( 14.78499923084727286, -30.41584920728202235, -24.59895335003452743 ) ) ;
#11355=CARTESIAN_POINT ( 'NONE',  ( 14.72842623554610419, -21.99999999999999645, -26.93849963251682311 ) ) ;
#11383=ORIENTED_EDGE ( 'NONE', *, *, #673, .T. ) ;
#11451=DIRECTION ( 'NONE',  ( 0.000000000000000000, 1.000000000000000000, 0.000000000000000000 ) ) ;
#11460=ORIENTED_EDGE ( 'NONE', *, *, #64, .T. ) ;
#11467=ADVANCED_FACE ( 'NONE', ( #23619 ), #26041, .T. ) ;
#11509=CARTESIAN_POINT ( 'NONE',  ( 14.81428820541019142, -22.00000000000000711, -27.51054546844379445 ) ) ;
#11539=VERTEX_POINT ( 'NONE', #30264 ) ;
#11576=SURFACE_STYLE_FILL_AREA ( #1987 ) ;
#11624=DIRECTION ( 'NONE',  ( 0.000000000000000000, -0.5000000000001900702, -0.8660254037843290176 ) ) ;
#11662=CARTESIAN_POINT ( 'NONE',  ( 14.75563848642255849, -22.00000000000000000, -29.68302488264445671 ) ) ;
#11755=EDGE_CURVE ( 'NONE', #12454, #6451, #10465, .T. ) ;
#11864=ORIENTED_EDGE ( 'NONE', *, *, #1101, .T. ) ;
#11963=ORIENTED_EDGE ( 'NONE', *, *, #14798, .T. ) ;
#11983=CARTESIAN_POINT ( 'NONE',  ( 14.54393567127463172, -26.57411906178515082, -22.87237978256219151 ) ) ;
#12049=DIRECTION ( 'NONE',  ( 0.000000000000000000, 0.000000000000000000, 1.000000000000000000 ) ) ;
#12129=FACE_OUTER_BOUND ( 'NONE', #1944, .T. ) ;
#12154=AXIS2_PLACEMENT_3D ( 'NONE', #29229, #5623, #2959 ) ;
#12169=EDGE_CURVE ( 'NONE', #2554, #9917, #13998, .T. ) ;
#12231=CONICAL_SURFACE ( 'NONE', #19273, 4.997501249379996402, 1.047197551199999799 ) ;
#12244=DIRECTION ( 'NONE',  ( 1.000000000000000000, 0.000000000000000000, 0.000000000000000000 ) ) ;
#12281=MECHANICAL_DESIGN_GEOMETRIC_PRESENTATION_REPRESENTATION('',(#5739),#28855);
#12282=ORIENTED_EDGE ( 'NONE', *, *, #23155, .F. ) ;
#12454=VERTEX_POINT ( 'NONE', #17797 ) ;
#12600=VERTEX_POINT ( 'NONE', #19679 ) ;
#12645=DIRECTION ( 'NONE',  ( 0.4999999999969509945, 0.4151946956549595336, 0.7600087925169251024 ) ) ;
#12660=DIRECTION ( 'NONE',  ( 0.000000000000000000, -0.5000000000001900702, 0.8660254037843290176 ) ) ;
#12750=B_SPLINE_CURVE_WITH_KNOTS ( 'NONE', 3,
 ( #18105, #28024, #26144, #3959, #11194, #11355, #30707, #20951, #11509, #14032, #15913, #8985, #8824, #13712, #18585, #11662, #4113, #9134, #23786, #9295 ),
 .UNSPECIFIED., .F., .F.,
 ( 4, 1, 1, 1, 2, 2, 2, 1, 1, 1, 2, 2, 4 ),
 ( 0.000000000000000000, 0.1249999999999973910, 0.1874999999999968081, 0.2187499999999964195, 0.2343749999999971689, 0.2499999999999978906, 0.4999999999999924505, 0.6249999999999906741, 0.6874999999999898970, 0.7187499999999884537, 0.7343749999999886757, 0.7499999999999888978, 1.000000000000000000 ),
 .UNSPECIFIED. ) ;
#12769=ADVANCED_FACE ( 'NONE', ( #9884 ), #14614, .T. ) ;
#12797=VERTEX_POINT ( 'NONE', #610 ) ;
#12840=DIRECTION ( 'NONE',  ( 0.000000000000000000, -0.8660254037590263687, -0.5000000000440152359 ) ) ;
#12873=DIRECTION ( 'NONE',  ( -1.000000000000000000, 0.000000000000000000, 0.000000000000000000 ) ) ;
#12888=ORIENTED_EDGE ( 'NONE', *, *, #9351, .F. ) ;
#12894=DIRECTION ( 'NONE',  ( 0.000000000000000000, 0.000000000000000000, -1.000000000000000000 ) ) ;
#13050=FACE_OUTER_BOUND ( 'NONE', #25129, .T. ) ;
#13099=ORIENTED_EDGE ( 'NONE', *, *, #18735, .T. ) ;
#13123=CARTESIAN_POINT ( 'NONE',  ( 14.78339330455285960, -30.42684276135835830, -32.19501410105780081 ) ) ;
#13173=CONICAL_SURFACE ( 'NONE', #9664, 0.9999999999991022737, 0.7853981633970000820 ) ;
#13192=VECTOR ( 'NONE', #29044, 1000.000000000000114 ) ;
#13276=( GEOMETRIC_REPRESENTATION_CONTEXT ( 3 ) GLOBAL_UNCERTAINTY_ASSIGNED_CONTEXT ( ( #7173 ) ) GLOBAL_UNIT_ASSIGNED_CONTEXT ( ( #3868, #23075, #23548 ) ) REPRESENTATION_CONTEXT ( 'NONE', 'WORKASPACE' ) );
#13288=AXIS2_PLACEMENT_3D ( 'NONE', #20578, #11299, #6416 ) ;
#13339=CARTESIAN_POINT ( 'NONE',  ( 14.85086212533906469, -24.40458379250578247, -24.12496155405706588 ) ) ;
#13340=CARTESIAN_POINT ( 'NONE',  ( 14.54973694814395913, -27.44328476931316274, -33.91757211090763491 ) ) ;
#13357=DIRECTION ( 'NONE',  ( 0.000000000000000000, -0.8660254037843289066, 0.5000000000001899592 ) ) ;
#13427=EDGE_CURVE ( 'NONE', #15990, #12600, #9112, .T. ) ;
#13435=ADVANCED_FACE ( 'NONE', ( #20211 ), #29803, .T. ) ;
#13460=DIRECTION ( 'NONE',  ( 1.000000000000000000, 0.000000000000000000, 0.000000000000000000 ) ) ;
#13493=CARTESIAN_POINT ( 'NONE',  ( 14.80644526029530539, -28.75091651964295991, -33.16236467793404330 ) ) ;
#13513=LINE ( 'NONE', #27511, #30017 ) ;
#13518=B_SPLINE_CURVE_WITH_KNOTS ( 'NONE', 3,
 ( #24717, #14667, #19851, #5056, #19541, #15119, #7868, #28808, #17472, #27078, #11983, #29124 ),
 .UNSPECIFIED., .F., .F.,
 ( 4, 2, 2, 2, 2, 4 ),
 ( 0.000000000000000000, 0.2499999999999932276, 0.3749999999999916178, 0.4374999999999923395, 0.4999999999999931166, 1.000000000000000000 ),
 .UNSPECIFIED. ) ;
#13565=CARTESIAN_POINT ( 'NONE',  ( -18.29999999989999893, -29.92682926828999967, -28.39999999989999679 ) ) ;
#13583=EDGE_CURVE ( 'NONE', #24581, #9016, #5467, .T. ) ;
#13624=CARTESIAN_POINT ( 'NONE',  ( 14.75111860152068033, -23.36471428914778059, -32.07437842398911698 ) ) ;
#13668=CARTESIAN_POINT ( 'NONE',  ( 14.65905325912680013, -27.90098191447954434, -23.14712954807390588 ) ) ;
#13688=DIRECTION ( 'NONE',  ( -1.000000000000000000, 0.000000000000000000, 0.000000000000000000 ) ) ;
#13695=CARTESIAN_POINT ( 'NONE',  ( 11.20000000009999930, -24.49999999969999820, -32.73012701864999485 ) ) ;
#13712=CARTESIAN_POINT ( 'NONE',  ( 14.77490805647873273, -21.99999999999999645, -29.54211979042643677 ) ) ;
#13762=DIRECTION ( 'NONE',  ( 0.000000000000000000, 1.000000000000000000, 0.000000000000000000 ) ) ;
#13768=( NAMED_UNIT ( * ) PLANE_ANGLE_UNIT ( ) SI_UNIT ( $, .RADIAN. ) );
#13774=EDGE_CURVE ( 'NONE', #23742, #10372, #10433, .T. ) ;
#13785=VECTOR ( 'NONE', #4908, 1000.000000000000114 ) ;
#13792=CIRCLE ( 'NONE', #242, 2.926829268290000119 ) ;
#13935=AXIS2_PLACEMENT_3D ( 'NONE', #2304, #18807, #9528 ) ;
#13986=CARTESIAN_POINT ( 'NONE',  ( 14.47923079777483579, -27.23176631820642868, -22.76030765420599167 ) ) ;
#13996=VERTEX_POINT ( 'NONE', #13565 ) ;
#13998=CIRCLE ( 'NONE', #8975, 0.2500000000000002220 ) ;
#14015=DIRECTION ( 'NONE',  ( 0.000000000000000000, 0.000000000000000000, 1.000000000000000000 ) ) ;
#14032=CARTESIAN_POINT ( 'NONE',  ( 14.84786676130553573, -21.99999999999998934, -27.95750568651506995 ) ) ;
#14124=CARTESIAN_POINT ( 'NONE',  ( 10.70000000009999930, -30.05766787393000072, -27.53807693019799530 ) ) ;
#14132=ADVANCED_FACE ( 'NONE', ( #22314 ), #7374, .T. ) ;
#14198=CARTESIAN_POINT ( 'NONE',  ( 14.85000000009999788, -27.00000000000000000, -28.39999999989999679 ) ) ;
#14202=DIRECTION ( 'NONE',  ( 0.000000000000000000, 0.000000000000000000, -1.000000000000000000 ) ) ;
#14272=DIRECTION ( 'NONE',  ( 0.000000000000000000, -1.000000000000000000, 0.000000000000000000 ) ) ;
#14299=DIRECTION ( 'NONE',  ( 0.000000000000000000, 1.000000000000000000, 0.000000000000000000 ) ) ;
#14499=CARTESIAN_POINT ( 'NONE',  ( 12.80098767942999771, -32.00000000058999916, -25.51324865428999900 ) ) ;
#14523=ORIENTED_EDGE ( 'NONE', *, *, #6006, .F. ) ;
#14557=EDGE_CURVE ( 'NONE', #16714, #25254, #11012, .T. ) ;
#14614=CYLINDRICAL_SURFACE ( 'NONE', #15487, 4.439999999999999503 ) ;
#14647=LINE ( 'NONE', #14951, #4225 ) ;
#14660=DIRECTION ( 'NONE',  ( -1.075528555106586974E-13, -0.9622309798138365400, -0.2722343503059523884 ) ) ;
#14667=CARTESIAN_POINT ( 'NONE',  ( 14.84469677950085398, -24.79650568944878941, -23.89868534099636577 ) ) ;
#14777=TOROIDAL_SURFACE ( 'NONE', #18293, 3.176829268290000563, 0.2500000000000000000 ) ;
#14798=EDGE_CURVE ( 'NONE', #29336, #7923, #25599, .T. ) ;
#14896=DIRECTION ( 'NONE',  ( 1.000000000000000000, 0.000000000000000000, 0.000000000000000000 ) ) ;
#14932=FACE_OUTER_BOUND ( 'NONE', #24191, .T. ) ;
#14935=LINE ( 'NONE', #24533, #30346 ) ;
#14946=VECTOR ( 'NONE', #7095, 1000.000000000000000 ) ;
#14951=CARTESIAN_POINT ( 'NONE',  ( 12.80098767942999771, -27.00000000059169736, -22.62649730765999578 ) ) ;
#15119=CARTESIAN_POINT ( 'NONE',  ( 14.76986634514344310, -25.51951968493025902, -23.48139095529251463 ) ) ;
#15131=EDGE_LOOP ( 'NONE', ( #25939, #11460, #27179 ) ) ;
#15164=AXIS2_PLACEMENT_3D ( 'NONE', #17916, #22814, #15266 ) ;
#15179=CARTESIAN_POINT ( 'NONE',  ( 14.68395928812360651, -31.04325972095271169, -31.83912560350277943 ) ) ;
#15240=CONICAL_SURFACE ( 'NONE', #19789, 4.997501249379996402, 1.047197551199999799 ) ;
#15251=FACE_OUTER_BOUND ( 'NONE', #10340, .T. ) ;
#15266=DIRECTION ( 'NONE',  ( 0.000000000000000000, 1.000000000000000000, 0.000000000000000000 ) ) ;
#15276=DIRECTION ( 'NONE',  ( 1.000000000000000000, 0.000000000000000000, 0.000000000000000000 ) ) ;
#15342=CARTESIAN_POINT ( 'NONE',  ( 14.75111860151799270, -31.99974791380525474, -29.71106056348426705 ) ) ;
#15386=DIRECTION ( 'NONE',  ( 0.000000000000000000, 1.000000000000000000, 0.000000000000000000 ) ) ;
#15487=AXIS2_PLACEMENT_3D ( 'NONE', #24059, #2803, #17420 ) ;
#15491=CARTESIAN_POINT ( 'NONE',  ( 14.77204036655766650, -30.50348270133963169, -32.15076601107894305 ) ) ;
#15507=CARTESIAN_POINT ( 'NONE',  ( 14.69473318574859455, -25.93431317557370619, -33.55782932027766208 ) ) ;
#15531=ADVANCED_BREP_SHAPE_REPRESENTATION ( '', ( #21644, #17722 ), #13276 ) ;
#15568=CARTESIAN_POINT ( 'NONE',  ( 14.85000000009999788, -27.00000000000000000, -28.39999999989999679 ) ) ;
#15589=PRODUCT_DEFINITION_SHAPE ( 'NONE', 'NONE',  #54 ) ;
#15605=CARTESIAN_POINT ( 'NONE',  ( 353532.1637640000554, -340227.0254469999345, -96277.77758659989922 ) ) ;
#15662=PLANE ( 'NONE',  #29768 ) ;
#15739=B_SPLINE_CURVE_WITH_KNOTS ( 'NONE', 3,
 ( #3739, #13339, #3900, #20735, #15860, #18202, #8924, #4057, #30336, #27810, #11139 ),
 .UNSPECIFIED., .F., .F.,
 ( 4, 1, 1, 1, 2, 2, 4 ),
 ( 0.000000000000000000, 0.2499999999999913958, 0.3749999999999870659, 0.4374999999999865663, 0.4687499999999862887, 0.4999999999999860112, 1.000000000000000000 ),
 .UNSPECIFIED. ) ;
#15749=DIRECTION ( 'NONE',  ( 0.000000000000000000, -1.000000000000000000, 0.000000000000000000 ) ) ;
#15778=B_SPLINE_CURVE_WITH_KNOTS ( 'NONE', 3,
 ( #23570, #2004, #17229, #29184, #7631, #10160, #26832, #19603, #29341, #29500, #5429, #5117, #7786, #9848, #7937, #22119, #17388, #3371, #3219, #24940, #24785, #15342, #5285, #26991, #5737, #10319 ),
 .UNSPECIFIED., .F., .F.,
 ( 4, 2, 2, 1, 1, 2, 2, 2, 2, 2, 1, 1, 2, 2, 4 ),
 ( 0.000000000000000000, 0.1249999999999930611, 0.1874999999999903133, 0.2187499999999897304, 0.2343749999999894529, 0.2421874999999900913, 0.2499999999999907296, 0.4999999999999993339, 0.6250000000000036637, 0.6875000000000068834, 0.7187500000000075495, 0.7343750000000088818, 0.7421875000000085487, 0.7500000000000082157, 1.000000000000000000 ),
 .UNSPECIFIED. ) ;
#15787=AXIS2_PLACEMENT_3D ( 'NONE', #28359, #9474, #14202 ) ;
#15790=VERTEX_POINT ( 'NONE', #1574 ) ;
#15808=CARTESIAN_POINT ( 'NONE',  ( 14.85086212533918548, -29.59541620749952884, -32.67503844573987237 ) ) ;
#15860=CARTESIAN_POINT ( 'NONE',  ( 14.78339330455186662, -23.57315723864463308, -24.60498589874045194 ) ) ;
#15861=CARTESIAN_POINT ( 'NONE',  ( 14.74534393132121579, -28.33174258796800871, -33.40462800574894686 ) ) ;
#15902=CARTESIAN_POINT ( 'NONE',  ( 12.80098767942999771, -22.00000000000000000, -25.51324865327000069 ) ) ;
#15913=CARTESIAN_POINT ( 'NONE',  ( 14.84798480953660338, -22.00000000000000355, -28.62014973081917191 ) ) ;
#15928=VECTOR ( 'NONE', #26060, 1000.000000000000227 ) ;
#15937=ORIENTED_EDGE ( 'NONE', *, *, #14557, .F. ) ;
#15982=CARTESIAN_POINT ( 'NONE',  ( 14.75521759265608424, -23.38921439669723057, -32.08852866628550515 ) ) ;
#15990=VERTEX_POINT ( 'NONE', #25613 ) ;
#16004=DIRECTION ( 'NONE',  ( -1.000000000000000000, 0.000000000000000000, 0.000000000000000000 ) ) ;
#16013=CARTESIAN_POINT ( 'NONE',  ( 14.83413420727321963, -29.02780189700713365, -33.00248536946025979 ) ) ;
#16025=CARTESIAN_POINT ( 'NONE',  ( 14.84835410051194948, -29.11010934775363523, -23.84443905029603172 ) ) ;
#16053=ORIENTED_EDGE ( 'NONE', *, *, #7866, .T. ) ;
#16163=EDGE_CURVE ( 'NONE', #28640, #12600, #15778, .T. ) ;
#16175=SHAPE_DEFINITION_REPRESENTATION ( #15589, #20820 ) ;
#16181=CARTESIAN_POINT ( 'NONE',  ( 14.77468706462270376, -30.48866542731327911, -24.64097061684832468 ) ) ;
#16258=CARTESIAN_POINT ( 'NONE',  ( 12.80098767942999771, -32.00000000000000000, -31.28675134584999640 ) ) ;
#16269=ORIENTED_EDGE ( 'NONE', *, *, #17127, .F. ) ;
#16362=DIRECTION ( 'NONE',  ( 1.000000000000000000, -1.381176317861079950E-13, 9.436729139529790430E-14 ) ) ;
#16451=CARTESIAN_POINT ( 'NONE',  ( -249983.7073439999076, 207571.5457919999899, 379978.1891180000966 ) ) ;
#16483=ORIENTED_EDGE ( 'NONE', *, *, #14557, .T. ) ;
#16487=CARTESIAN_POINT ( 'NONE',  ( 14.81460958102700332, -30.17431306372085231, -24.45952979736321353 ) ) ;
#16621=LINE ( 'NONE', #11166, #13192 ) ;
#16714=VERTEX_POINT ( 'NONE', #23793 ) ;
#16804=EDGE_LOOP ( 'NONE', ( #25028, #27231, #19372, #30513 ) ) ;
#16934=ADVANCED_FACE ( 'NONE', ( #13050 ), #13173, .T. ) ;
#16951=ORIENTED_EDGE ( 'NONE', *, *, #23155, .T. ) ;
#16961=EDGE_LOOP ( 'NONE', ( #9241, #11383, #18686, #20266, #4909 ) ) ;
#17017=FACE_OUTER_BOUND ( 'NONE', #16804, .T. ) ;
#17120=DIRECTION ( 'NONE',  ( -0.000000000000000000, 1.000000000000000000, 0.000000000000000000 ) ) ;
#17127=EDGE_CURVE ( 'NONE', #9871, #4371, #16621, .T. ) ;
#17132=ORIENTED_EDGE ( 'NONE', *, *, #1351, .T. ) ;
#17229=CARTESIAN_POINT ( 'NONE',  ( 14.54659216920905962, -31.99974211811322533, -26.04155240325682641 ) ) ;
#17337=ORIENTED_EDGE ( 'NONE', *, *, #5548, .T. ) ;
#17378=CARTESIAN_POINT ( 'NONE',  ( 11.20000000009999930, -22.00000000000000000, -25.51324865394999719 ) ) ;
#17388=CARTESIAN_POINT ( 'NONE',  ( 14.80403571754988512, -31.99970031113917557, -29.28999737812765147 ) ) ;
#17420=DIRECTION ( 'NONE',  ( 0.000000000000000000, 1.000000000000000000, 0.000000000000000000 ) ) ;
#17472=CARTESIAN_POINT ( 'NONE',  ( 14.73745037969879590, -25.71390008926000448, -23.36904195206612656 ) ) ;
#17722=AXIS2_PLACEMENT_3D ( 'NONE', #2627, #14015, #29203 ) ;
#17786=AXIS2_PLACEMENT_3D ( 'NONE', #26465, #358, #2699 ) ;
#17797=CARTESIAN_POINT ( 'NONE',  ( -19.29999999990000248, -28.92682926916000241, -28.39999999989999679 ) ) ;
#17856=CARTESIAN_POINT ( 'NONE',  ( 14.74203063448154793, -25.68810651402014500, -33.41580572993174059 ) ) ;
#17874=EDGE_CURVE ( 'NONE', #19357, #30733, #3004, .T. ) ;
#17916=CARTESIAN_POINT ( 'NONE',  ( 14.85000000009999788, -27.00000000000000000, -28.39999999989999679 ) ) ;
#17975=ORIENTED_EDGE ( 'NONE', *, *, #25218, .F. ) ;
#18012=CARTESIAN_POINT ( 'NONE',  ( 14.63279312439965274, -26.20928159737690066, -33.71653667584794078 ) ) ;
#18044=CARTESIAN_POINT ( 'NONE',  ( 14.66141101274631353, -27.86484103574591131, -33.67412216602015462 ) ) ;
#18054=ADVANCED_FACE ( 'NONE', ( #6600 ), #4090, .T. ) ;
#18105=CARTESIAN_POINT ( 'NONE',  ( 14.40197535836999876, -22.00000000000000000, -25.51324865394999719 ) ) ;
#18140=ORIENTED_EDGE ( 'NONE', *, *, #673, .F. ) ;
#18185=LINE ( 'NONE', #21184, #10538 ) ;
#18202=CARTESIAN_POINT ( 'NONE',  ( 14.77204036655656338, -23.49651729866158334, -24.64923398872036842 ) ) ;
#18216=CARTESIAN_POINT ( 'NONE',  ( 14.67158610511795480, -31.09694805760351244, -24.99235543444519081 ) ) ;
#18238=EDGE_CURVE ( 'NONE', #16714, #2554, #5677, .T. ) ;
#18293=AXIS2_PLACEMENT_3D ( 'NONE', #5293, #14896, #737 ) ;
#18296=COLOUR_RGB ( '', 0.72549020, 0.75294118, 0.79215686) ;
#18299=ORIENTED_EDGE ( 'NONE', *, *, #21926, .T. ) ;
#18300=AXIS2_PLACEMENT_3D ( 'NONE', #27415, #844, #27264 ) ;
#18312=MECHANICAL_DESIGN_GEOMETRIC_PRESENTATION_REPRESENTATION('',(#25351),#30386);
#18340=FILL_AREA_STYLE_COLOUR ( '', #3235 ) ;
#18348=ADVANCED_FACE ( 'NONE', ( #1387 ), #25139, .T. ) ;
#18411=DIRECTION ( 'NONE',  ( 0.000000000000000000, 0.8660254037843289066, 0.5000000000001899592 ) ) ;
#18459=ORIENTED_EDGE ( 'NONE', *, *, #13774, .T. ) ;
#18497=PRESENTATION_STYLE_ASSIGNMENT (( #28410 ) ) ;
#18527=CARTESIAN_POINT ( 'NONE',  ( 14.79527398937326410, -28.65846030549727175, -33.21580101399630536 ) ) ;
#18540=CARTESIAN_POINT ( 'NONE',  ( 14.84842474946386126, -29.69419767703834623, -24.18168994580233289 ) ) ;
#18574=VECTOR ( 'NONE', #12049, 1000.000000000000000 ) ;
#18585=CARTESIAN_POINT ( 'NONE',  ( 14.76350381782003218, -21.99999999999998934, -29.62663954576006020 ) ) ;
#18654=ORIENTED_EDGE ( 'NONE', *, *, #10073, .T. ) ;
#18686=ORIENTED_EDGE ( 'NONE', *, *, #204, .T. ) ;
#18691=CARTESIAN_POINT ( 'NONE',  ( 14.74466352505200284, -28.32694284507041260, -23.39287652031412179 ) ) ;
#18735=EDGE_CURVE ( 'NONE', #4103, #19446, #23223, .T. ) ;
#18807=DIRECTION ( 'NONE',  ( -1.000000000000000000, 0.000000000000000000, 0.000000000000000000 ) ) ;
#18853=CARTESIAN_POINT ( 'NONE',  ( 14.74203063447538753, -28.31189348597844102, -23.38419426985683813 ) ) ;
#18857=DIRECTION ( 'NONE',  ( 0.000000000000000000, 1.000000000000000000, 0.000000000000000000 ) ) ;
#18909=DIRECTION ( 'NONE',  ( 0.000000000000000000, 0.4794255386042040601, 0.8775825618903722036 ) ) ;
#18959=CARTESIAN_POINT ( 'NONE',  ( 10.45000000009999930, -27.00000000000000000, -28.39999999989999679 ) ) ;
#19046=ORIENTED_EDGE ( 'NONE', *, *, #16163, .F. ) ;
#19055=CARTESIAN_POINT ( 'NONE',  ( 10.95000000009999930, -22.55999999999999872, -28.39999999989999679 ) ) ;
#19132=UNCERTAINTY_MEASURE_WITH_UNIT (LENGTH_MEASURE( 1.000000000000000082E-05 ), #22909, 'distance_accuracy_value', 'NONE');
#19273=AXIS2_PLACEMENT_3D ( 'NONE', #15568, #3611, #22980 ) ;
#19357=VERTEX_POINT ( 'NONE', #2692 ) ;
#19372=ORIENTED_EDGE ( 'NONE', *, *, #2583, .T. ) ;
#19446=VERTEX_POINT ( 'NONE', #7864 ) ;
#19469=ADVANCED_FACE ( 'NONE', ( #27680 ), #22660, .T. ) ;
#19541=CARTESIAN_POINT ( 'NONE',  ( 14.79116926529892417, -25.37390977572334450, -23.56557456066964917 ) ) ;
#19546=CARTESIAN_POINT ( 'NONE',  ( 11.20000000009999930, -32.00000000000000000, -25.51324865394999719 ) ) ;
#19603=CARTESIAN_POINT ( 'NONE',  ( 14.72975346148569287, -31.99973334780656486, -26.94935724806895294 ) ) ;
#19627=DIRECTION ( 'NONE',  ( 0.000000000000000000, 1.000000000000000000, 0.000000000000000000 ) ) ;
#19652=CARTESIAN_POINT ( 'NONE',  ( 10.45000000009999930, -27.00000000000000000, -28.39999999989999679 ) ) ;
#19679=CARTESIAN_POINT ( 'NONE',  ( 14.40197535836999876, -32.00000000000000000, -31.28675134584999640 ) ) ;
#19777=VERTEX_POINT ( 'NONE', #8128 ) ;
#19789=AXIS2_PLACEMENT_3D ( 'NONE', #14198, #28040, #18909 ) ;
#19829=PLANE ( 'NONE',  #30654 ) ;
#19851=CARTESIAN_POINT ( 'NONE',  ( 14.83319110805087071, -24.98846848000023613, -23.78818000047916925 ) ) ;
#19854=EDGE_LOOP ( 'NONE', ( #3962, #4256, #27172, #4770, #14523 ) ) ;
#19917=EDGE_CURVE ( 'NONE', #25371, #25254, #9080, .T. ) ;
#20013=DIRECTION ( 'NONE',  ( 1.000000000000000000, 0.000000000000000000, 0.000000000000000000 ) ) ;
#20211=FACE_OUTER_BOUND ( 'NONE', #28676, .T. ) ;
#20266=ORIENTED_EDGE ( 'NONE', *, *, #29145, .F. ) ;
#20353=AXIS2_PLACEMENT_3D ( 'NONE', #6150, #22539, #15749 ) ;
#20392=CARTESIAN_POINT ( 'NONE',  ( 14.81460958102759484, -23.82568693630179624, -32.34047020245367321 ) ) ;
#20464=CARTESIAN_POINT ( 'NONE',  ( -18.29999999989999893, -24.07317073171000033, -28.39999999989999679 ) ) ;
#20472=DIRECTION ( 'NONE',  ( 0.000000000000000000, 1.000000000000000000, 0.000000000000000000 ) ) ;
#20474=EDGE_CURVE ( 'NONE', #25571, #28640, #21426, .T. ) ;
#20499=AXIS2_PLACEMENT_3D ( 'NONE', #28834, #16362, #30106 ) ;
#20578=CARTESIAN_POINT ( 'NONE',  ( -18.29999999989999893, -27.00000000000000000, -28.39999999989999679 ) ) ;
#20615=CARTESIAN_POINT ( 'NONE',  ( 10.95000000009999930, -31.44000000000000128, -28.39999999989999679 ) ) ;
#20666=CARTESIAN_POINT ( 'NONE',  ( 14.40197535836999876, -22.00000000000000000, -31.28675134584999640 ) ) ;
#20686=CARTESIAN_POINT ( 'NONE',  ( 10.70000000009999930, -27.00000000000000000, -28.39999999989999679 ) ) ;
#20706=CARTESIAN_POINT ( 'NONE',  ( 14.55660443455961328, -22.46388722856030640, -31.55457676213481477 ) ) ;
#20719=DIRECTION ( 'NONE',  ( 1.000000000000000000, 0.000000000000000000, 0.000000000000000000 ) ) ;
#20735=CARTESIAN_POINT ( 'NONE',  ( 14.80686173019908125, -23.75137256601108149, -24.50209323151165108 ) ) ;
#20755=AXIS2_PLACEMENT_3D ( 'NONE', #19652, #29854, #8288 ) ;
#20813=ORIENTED_EDGE ( 'NONE', *, *, #782, .T. ) ;
#20820=SHAPE_REPRESENTATION ( 'Bolt M6', ( #17722 ), #13276 ) ;
#20864=SURFACE_STYLE_USAGE ( .BOTH. , #4019 ) ;
#20881=DIRECTION ( 'NONE',  ( -1.000000000000000000, 0.000000000000000000, 0.000000000000000000 ) ) ;
#20884=DIRECTION ( 'NONE',  ( 0.000000000000000000, -1.000000000000000000, 0.000000000000000000 ) ) ;
#20901=CARTESIAN_POINT ( 'NONE',  ( 14.77560465009611335, -28.51899377725004925, -33.29642281725517705 ) ) ;
#20951=CARTESIAN_POINT ( 'NONE',  ( 14.74301764161975825, -21.99999999999999289, -27.03153114797974865 ) ) ;
#20996=ORIENTED_EDGE ( 'NONE', *, *, #5968, .F. ) ;
#21015=SURFACE_STYLE_FILL_AREA ( #25583 ) ;
#21124=CIRCLE ( 'NONE', #7546, 4.439999999480002124 ) ;
#21183=DIRECTION ( 'NONE',  ( 0.000000000000000000, 0.5000000000001900702, -0.8660254037843290176 ) ) ;
#21184=CARTESIAN_POINT ( 'NONE',  ( 11.20000000009999930, -24.50000000030000180, -24.06987298079999604 ) ) ;
#21247=DIRECTION ( 'NONE',  ( 1.000000000000000000, 0.000000000000000000, 0.000000000000000000 ) ) ;
#21327=FACE_OUTER_BOUND ( 'NONE', #11308, .T. ) ;
#21329=( NAMED_UNIT ( * ) SI_UNIT ( $, .STERADIAN. ) SOLID_ANGLE_UNIT ( ) );
#21346=DIRECTION ( 'NONE',  ( 1.386461269282634800E-13, 1.000000000000000000, 0.000000000000000000 ) ) ;
#21352=CARTESIAN_POINT ( 'NONE',  ( 10.70000000009999930, -27.00000000000000000, -28.39999999989999679 ) ) ;
#21400=DIRECTION ( 'NONE',  ( 0.000000000000000000, 0.000000000000000000, 1.000000000000000000 ) ) ;
#21426=LINE ( 'NONE', #14499, #25695 ) ;
#21482=AXIS2_PLACEMENT_3D ( 'NONE', #22762, #20719, #20884 ) ;
#21552=CARTESIAN_POINT ( 'NONE',  ( -19.29999999990000248, -27.00000000000000000, -28.39999999989999679 ) ) ;
#21558=EDGE_LOOP ( 'NONE', ( #25874, #9625, #3312, #7300, #6746, #8854, #6971 ) ) ;
#21563=EDGE_CURVE ( 'NONE', #15790, #25571, #7642, .T. ) ;
#21644=MANIFOLD_SOLID_BREP ( 'PartBody', #6526 ) ;
#21683=EDGE_LOOP ( 'NONE', ( #25474, #16951, #30423, #2075 ) ) ;
#21926=EDGE_CURVE ( 'NONE', #6451, #23742, #29886, .T. ) ;
#21991=ORIENTED_EDGE ( 'NONE', *, *, #2583, .F. ) ;
#22039=ORIENTED_EDGE ( 'NONE', *, *, #22345, .F. ) ;
#22119=CARTESIAN_POINT ( 'NONE',  ( 14.81460958102601211, -31.99970383011995523, -29.17880065134524870 ) ) ;
#22263=VECTOR ( 'NONE', #5204, 1000.000000000000000 ) ;
#22298=EDGE_LOOP ( 'NONE', ( #9014, #16483, #9476, #4685 ) ) ;
#22300=VECTOR ( 'NONE', #15276, 1000.000000000000000 ) ;
#22314=FACE_OUTER_BOUND ( 'NONE', #2387, .T. ) ;
#22337=ORIENTED_EDGE ( 'NONE', *, *, #25218, .T. ) ;
#22345=EDGE_CURVE ( 'NONE', #13996, #1635, #5255, .T. ) ;
#22381=ORIENTED_EDGE ( 'NONE', *, *, #17127, .T. ) ;
#22453=ORIENTED_EDGE ( 'NONE', *, *, #11755, .F. ) ;
#22493=CIRCLE ( 'NONE', #384, 1.926829268289999231 ) ;
#22500=CARTESIAN_POINT ( 'NONE',  ( 11.20000000009999930, -27.00000000000000000, -28.39999999989999679 ) ) ;
#22539=DIRECTION ( 'NONE',  ( -1.000000000000000000, 0.000000000000000000, 0.000000000000000000 ) ) ;
#22565=AXIS2_PLACEMENT_3D ( 'NONE', #766, #17120, #12244 ) ;
#22632=CARTESIAN_POINT ( 'NONE',  ( 10.70000000009999930, -27.00000000000000000, -28.39999999989999679 ) ) ;
#22660=PLANE ( 'NONE',  #15164 ) ;
#22731=CARTESIAN_POINT ( 'NONE',  ( 14.56598578705985325, -31.50796871393007947, -31.57082574131231922 ) ) ;
#22751=CARTESIAN_POINT ( 'NONE',  ( 14.74466352505797673, -25.67305715492923213, -33.40712347947508931 ) ) ;
#22762=CARTESIAN_POINT ( 'NONE',  ( 10.95000000009999930, -27.00000000000000000, -28.39999999989999679 ) ) ;
#22814=DIRECTION ( 'NONE',  ( 1.000000000000000000, 0.000000000000000000, 0.000000000000000000 ) ) ;
#22841=CIRCLE ( 'NONE', #18300, 3.176829269159998859 ) ;
#22895=CARTESIAN_POINT ( 'NONE',  ( 14.76418395427435115, -30.55463420411378905, -32.12123367718280775 ) ) ;
#22909=( LENGTH_UNIT ( ) NAMED_UNIT ( * ) SI_UNIT ( .MILLI., .METRE. ) );
#22916=CARTESIAN_POINT ( 'NONE',  ( 14.77468706462266823, -23.51133457270864469, -32.15902938297210767 ) ) ;
#22954=B_SPLINE_CURVE_WITH_KNOTS ( 'NONE', 3,
 ( #4380, #13986, #25478, #2181, #13668, #23273, #9092, #30815, #28142, #18853, #18691, #28450, #16025, #18540, #1717, #16487, #6581, #11314, #16181, #26100, #3915, #30187, #8619, #18216, #25793, #4228 ),
 .UNSPECIFIED., .F., .F.,
 ( 4, 2, 2, 1, 1, 2, 2, 2, 2, 2, 1, 1, 2, 2, 4 ),
 ( 0.000000000000000000, 0.1250000000000079659, 0.1875000000000115463, 0.2187500000000133504, 0.2343750000000146549, 0.2421875000000145162, 0.2500000000000143774, 0.5000000000000217604, 0.6250000000000255351, 0.6875000000000281997, 0.7187500000000304201, 0.7343750000000323075, 0.7421875000000323075, 0.7500000000000323075, 1.000000000000000000 ),
 .UNSPECIFIED. ) ;
#22980=DIRECTION ( 'NONE',  ( 0.000000000000000000, -0.4794255386042040601, -0.8775825618903722036 ) ) ;
#23018=CARTESIAN_POINT ( 'NONE',  ( -19.29999999990000248, -28.85405481559000052, -28.92454911413899765 ) ) ;
#23075=( NAMED_UNIT ( * ) PLANE_ANGLE_UNIT ( ) SI_UNIT ( $, .RADIAN. ) );
#23155=EDGE_CURVE ( 'NONE', #4371, #19357, #28167, .T. ) ;
#23176=AXIS2_PLACEMENT_3D ( 'NONE', #23421, #1851, #11451 ) ;
#23223=CIRCLE ( 'NONE', #12154, 4.997501249380000843 ) ;
#23273=CARTESIAN_POINT ( 'NONE',  ( 14.69473318574057430, -28.06568682441304574, -23.24217067950538862 ) ) ;
#23282=ORIENTED_EDGE ( 'NONE', *, *, #437, .F. ) ;
#23404=ORIENTED_EDGE ( 'NONE', *, *, #14798, .F. ) ;
#23407=DIRECTION ( 'NONE',  ( 0.000000000000000000, 4.000204360710000258E-16, 1.000000000000000000 ) ) ;
#23421=CARTESIAN_POINT ( 'NONE',  ( 10.70000000009999930, -27.00000000000000000, -28.39999999989999679 ) ) ;
#23515=VECTOR ( 'NONE', #12894, 1000.000000000000000 ) ;
#23543=B_SPLINE_CURVE_WITH_KNOTS ( 'NONE', 3,
 ( #4210, #11298, #16013, #13493, #18527, #20901, #8925, #23582, #15861, #8603, #28129, #18044, #13340, #6415 ),
 .UNSPECIFIED., .F., .F.,
 ( 4, 2, 2, 1, 1, 2, 2, 4 ),
 ( 0.000000000000000000, 0.2500000000000140998, 0.3750000000000173750, 0.4375000000000172640, 0.4687500000000170974, 0.4843750000000187073, 0.5000000000000203171, 1.000000000000000000 ),
 .UNSPECIFIED. ) ;
#23548=( NAMED_UNIT ( * ) SI_UNIT ( $, .STERADIAN. ) SOLID_ANGLE_UNIT ( ) );
#23570=CARTESIAN_POINT ( 'NONE',  ( 14.40197535836999876, -32.00000000000000000, -25.51324865394999719 ) ) ;
#23582=CARTESIAN_POINT ( 'NONE',  ( 14.75144444200372718, -28.36701773692398731, -33.38425558406653693 ) ) ;
#23619=FACE_OUTER_BOUND ( 'NONE', #5861, .T. ) ;
#23742=VERTEX_POINT ( 'NONE', #23018 ) ;
#23767=ADVANCED_FACE ( 'NONE', ( #29353 ), #14777, .F. ) ;
#23772=CARTESIAN_POINT ( 'NONE',  ( 14.54659216921188936, -26.54260447311150628, -33.90912748487277639 ) ) ;
#23786=CARTESIAN_POINT ( 'NONE',  ( 14.56063207224778289, -22.00000000000000355, -30.73714836706114895 ) ) ;
#23793=CARTESIAN_POINT ( 'NONE',  ( 10.45000000009999930, -29.92682926828999967, -28.39999999990001811 ) ) ;
#23871=CARTESIAN_POINT ( 'NONE',  ( -19.29999999990000248, -26.99999999999986144, -28.39999999990009272 ) ) ;
#23966=ORIENTED_EDGE ( 'NONE', *, *, #18238, .T. ) ;
#23981=CARTESIAN_POINT ( 'NONE',  ( 11.20000000009999930, -27.00000000000000000, -28.39999999989999679 ) ) ;
#24059=CARTESIAN_POINT ( 'NONE',  ( 10.95000000009999930, -27.00000000000000000, -28.39999999989999679 ) ) ;
#24092=VECTOR ( 'NONE', #20881, 1000.000000000000000 ) ;
#24175=CARTESIAN_POINT ( 'NONE',  ( 10.45000000009999930, -30.17682926828999967, -28.39999999989999679 ) ) ;
#24191=EDGE_LOOP ( 'NONE', ( #26906, #28047 ) ) ;
#24382=CIRCLE ( 'NONE', #2774, 2.926829268290000119 ) ;
#24418=CARTESIAN_POINT ( 'NONE',  ( 353532.1637640000554, -353580.3905929999310, -28.39999994950992956 ) ) ;
#24517=ORIENTED_EDGE ( 'NONE', *, *, #25675, .T. ) ;
#24529=DIRECTION ( 'NONE',  ( 1.000000000000000000, 0.000000000000000000, 0.000000000000000000 ) ) ;
#24533=CARTESIAN_POINT ( 'NONE',  ( -4.299999999899999814, -29.92682926828999967, -28.39999999989999324 ) ) ;
#24563=DIRECTION ( 'NONE',  ( 1.000000000000000000, -1.381176317861079950E-13, 9.436729139529790430E-14 ) ) ;
#24572=EDGE_LOOP ( 'NONE', ( #27635, #17337, #24517, #1862 ) ) ;
#24581=VERTEX_POINT ( 'NONE', #8838 ) ;
#24652=ADVANCED_FACE ( 'NONE', ( #17017 ), #3743, .F. ) ;
#24670=EDGE_CURVE ( 'NONE', #12454, #13996, #2852, .T. ) ;
#24717=CARTESIAN_POINT ( 'NONE',  ( 14.84775334008999970, -24.60220466919999893, -24.01086508770000094 ) ) ;
#24785=CARTESIAN_POINT ( 'NONE',  ( 14.75521759265346589, -31.99975232932909108, -29.68276772680201603 ) ) ;
#24877=FACE_OUTER_BOUND ( 'NONE', #21558, .T. ) ;
#24916=ORIENTED_EDGE ( 'NONE', *, *, #11755, .T. ) ;
#24940=CARTESIAN_POINT ( 'NONE',  ( 14.76126683899760117, -31.99975590309085760, -29.64037414300432616 ) ) ;
#24958=CARTESIAN_POINT ( 'NONE',  ( 14.65905325913535684, -26.09901808550156943, -33.65287045170772728 ) ) ;
#24972=ORIENTED_EDGE ( 'NONE', *, *, #13427, .T. ) ;
#25028=ORIENTED_EDGE ( 'NONE', *, *, #64, .F. ) ;
#25129=EDGE_LOOP ( 'NONE', ( #1112, #2666, #3836, #22453 ) ) ;
#25139=CYLINDRICAL_SURFACE ( 'NONE', #26798, 2.926829268290000119 ) ;
#25148=ORIENTED_EDGE ( 'NONE', *, *, #20474, .T. ) ;
#25198=ADVANCED_FACE ( 'NONE', ( #626, #14932 ), #10833, .F. ) ;
#25215=DIRECTION ( 'NONE',  ( 0.000000000000000000, -1.000000000000000000, 0.000000000000000000 ) ) ;
#25218=EDGE_CURVE ( 'NONE', #15990, #5093, #23543, .T. ) ;
#25252=CARTESIAN_POINT ( 'NONE',  ( 14.76039189740110658, -30.57853635232509504, -32.10743376547878825 ) ) ;
#25254=VERTEX_POINT ( 'NONE', #25304 ) ;
#25264=FILL_AREA_STYLE_COLOUR ( '', #18296 ) ;
#25270=DIRECTION ( 'NONE',  ( -0.000000000000000000, 0.5000000000001900702, 0.8660254037843290176 ) ) ;
#25304=CARTESIAN_POINT ( 'NONE',  ( 10.70000000009999930, -30.17682926915999886, -28.39999999989999679 ) ) ;
#25351=STYLED_ITEM ( 'NONE', ( #18497 ), #15531 ) ;
#25371=VERTEX_POINT ( 'NONE', #14124 ) ;
#25414=PRODUCT_DEFINITION_CONTEXT ( 'detailed design', #9379, 'design' ) ;
#25419=CARTESIAN_POINT ( 'NONE',  ( 14.80686173019985219, -30.24862743399516063, -32.29790676828473295 ) ) ;
#25430=PRODUCT_DEFINITION_FORMATION_WITH_SPECIFIED_SOURCE ( 'ANY', '', #6042, .NOT_KNOWN. ) ;
#25438=CARTESIAN_POINT ( 'NONE',  ( 14.73716614373068801, -25.71543255174850984, -33.43156970936686889 ) ) ;
#25474=ORIENTED_EDGE ( 'NONE', *, *, #3129, .F. ) ;
#25478=CARTESIAN_POINT ( 'NONE',  ( 14.54659216920487452, -27.45739552686597307, -22.89087251491314845 ) ) ;
#25531=AXIS2_PLACEMENT_3D ( 'NONE', #6834, #4170, #13762 ) ;
#25571=VERTEX_POINT ( 'NONE', #19546 ) ;
#25583=FILL_AREA_STYLE ('',( #25264 ) ) ;
#25593=CARTESIAN_POINT ( 'NONE',  ( 14.71164558018262980, -25.85213278945484205, -33.51042165666717665 ) ) ;
#25599=CIRCLE ( 'NONE', #25531, 4.439999999480002124 ) ;
#25613=CARTESIAN_POINT ( 'NONE',  ( 14.84775334008999970, -29.39779533080000107, -32.78913491209999620 ) ) ;
#25675=EDGE_CURVE ( 'NONE', #24581, #29336, #5520, .T. ) ;
#25695=VECTOR ( 'NONE', #9452, 1000.000000000000000 ) ;
#25793=CARTESIAN_POINT ( 'NONE',  ( 14.55660443456689812, -31.53611277141912694, -25.24542323765480845 ) ) ;
#25874=ORIENTED_EDGE ( 'NONE', *, *, #16163, .T. ) ;
#25939=ORIENTED_EDGE ( 'NONE', *, *, #5968, .T. ) ;
#25951=FACE_OUTER_BOUND ( 'NONE', #9873, .T. ) ;
#25974=LINE ( 'NONE', #15902, #27640 ) ;
#26009=FACE_OUTER_BOUND ( 'NONE', #29278, .T. ) ;
#26041=CONICAL_SURFACE ( 'NONE', #20499, 0.9999999999991012745, 0.7853981633970000820 ) ;
#26055=CARTESIAN_POINT ( 'NONE',  ( 14.84775334008999970, -24.60220466919999893, -24.01086508770000094 ) ) ;
#26060=DIRECTION ( 'NONE',  ( 0.4999999999969509945, -0.4151946956549595336, -0.7600087925169251024 ) ) ;
#26069=CARTESIAN_POINT ( 'NONE',  ( 11.20000000009999930, -27.00000000000000000, -34.17350269180000311 ) ) ;
#26100=CARTESIAN_POINT ( 'NONE',  ( 14.76126683900035985, -30.57407346967977446, -24.69027144666924301 ) ) ;
#26132=EDGE_CURVE ( 'NONE', #16714, #13996, #14935, .T. ) ;
#26144=CARTESIAN_POINT ( 'NONE',  ( 14.58373518890417486, -21.99999999999999645, -26.18669965537439026 ) ) ;
#26169=ORIENTED_EDGE ( 'NONE', *, *, #10425, .F. ) ;
#26215=LINE ( 'NONE', #4819, #24092 ) ;
#26335=LINE ( 'NONE', #26482, #10521 ) ;
#26336=CARTESIAN_POINT ( 'NONE',  ( 10.45000000009999930, -30.05766787309999799, -27.53807693043399851 ) ) ;
#26465=CARTESIAN_POINT ( 'NONE',  ( 10.45000000009999930, -26.99999999999950617, -28.39999999990030588 ) ) ;
#26482=CARTESIAN_POINT ( 'NONE',  ( 12.80098767942999771, -26.99999999940830264, -34.17350269213999781 ) ) ;
#26557=DIRECTION ( 'NONE',  ( 1.000000000000000000, 0.000000000000000000, 0.000000000000000000 ) ) ;
#26602=AXIS2_PLACEMENT_3D ( 'NONE', #26336, #7442, #7742 ) ;
#26798=AXIS2_PLACEMENT_3D ( 'NONE', #29704, #12873, #3419 ) ;
#26810=DIRECTION ( 'NONE',  ( 1.386461269282634800E-13, 1.000000000000000000, 0.000000000000000000 ) ) ;
#26832=CARTESIAN_POINT ( 'NONE',  ( 14.71164558017381019, -31.99968858407690320, -26.83887133594891239 ) ) ;
#26906=ORIENTED_EDGE ( 'NONE', *, *, #13583, .F. ) ;
#26952=ADVANCED_FACE ( 'NONE', ( #21327 ), #2696, .F. ) ;
#26974=CARTESIAN_POINT ( 'NONE',  ( -249983.7073439999076, -207625.5457919999608, -380034.9891179999686 ) ) ;
#26991=CARTESIAN_POINT ( 'NONE',  ( 14.67158610510948513, -31.99958078956481700, -30.24423881306254813 ) ) ;
#27078=CARTESIAN_POINT ( 'NONE',  ( 14.65261876681249120, -26.16807071656643657, -23.10688672985826742 ) ) ;
#27172=ORIENTED_EDGE ( 'NONE', *, *, #26132, .T. ) ;
#27179=ORIENTED_EDGE ( 'NONE', *, *, #19917, .T. ) ;
#27213=FACE_BOUND ( 'NONE', #2024, .T. ) ;
#27231=ORIENTED_EDGE ( 'NONE', *, *, #12169, .F. ) ;
#27249=CARTESIAN_POINT ( 'NONE',  ( 10.45000000009999930, -26.99999999999950617, -28.39999999990030588 ) ) ;
#27264=DIRECTION ( 'NONE',  ( 0.000000000000000000, 1.000000000000000000, 0.000000000000000000 ) ) ;
#27294=CARTESIAN_POINT ( 'NONE',  ( 14.84171152945997640, -29.89464157630768781, -32.50228059851001206 ) ) ;
#27367=DIRECTION ( 'NONE',  ( 0.7071067811870476172, 0.7071067811860475283, -3.047758891780202378E-14 ) ) ;
#27378=DIRECTION ( 'NONE',  ( 1.000000000000000000, -1.317089015970003879E-16, -1.110223024630000146E-15 ) ) ;
#27402=DIRECTION ( 'NONE',  ( 1.000000000000000000, 0.000000000000000000, 0.000000000000000000 ) ) ;
#27415=CARTESIAN_POINT ( 'NONE',  ( 10.70000000009999930, -27.00000000000000000, -28.39999999989999679 ) ) ;
#27463=CARTESIAN_POINT ( 'NONE',  ( 11.20000000009999930, -22.00000000000000000, -25.51324865394999719 ) ) ;
#27511=CARTESIAN_POINT ( 'NONE',  ( 353532.1637640000554, 353526.3905929999892, -28.40000001513906724 ) ) ;
#27619=CARTESIAN_POINT ( 'NONE',  ( 14.81448010921499225, -25.26807234752766718, -33.17346377528555479 ) ) ;
#27630=FACE_OUTER_BOUND ( 'NONE', #29686, .T. ) ;
#27635=ORIENTED_EDGE ( 'NONE', *, *, #7956, .F. ) ;
#27640=VECTOR ( 'NONE', #21247, 1000.000000000000000 ) ;
#27680=FACE_OUTER_BOUND ( 'NONE', #9165, .T. ) ;
#27736=ORIENTED_EDGE ( 'NONE', *, *, #5, .T. ) ;
#27775=SHAPE_REPRESENTATION_RELATIONSHIP ( 'NONE' , 'NONE' ,  #20820, #15531 ) ;
#27810=CARTESIAN_POINT ( 'NONE',  ( 14.56598578705916225, -22.49203128606118440, -25.22917425849270501 ) ) ;
#27830=PLANE ( 'NONE',  #29020 ) ;
#27867=AXIS2_PLACEMENT_3D ( 'NONE', #29633, #9982, #26810 ) ;
#28024=CARTESIAN_POINT ( 'NONE',  ( 14.48117849943559499, -22.00000000000000000, -25.78761638283549118 ) ) ;
#28040=DIRECTION ( 'NONE',  ( -1.000000000000000000, 0.000000000000000000, 0.000000000000000000 ) ) ;
#28046=AXIS2_PLACEMENT_3D ( 'NONE', #4229, #6582, #14299 ) ;
#28047=ORIENTED_EDGE ( 'NONE', *, *, #5548, .F. ) ;
#28129=CARTESIAN_POINT ( 'NONE',  ( 14.73935963153661532, -28.29773402607040467, -33.42426426252703919 ) ) ;
#28142=CARTESIAN_POINT ( 'NONE',  ( 14.73716614372425049, -28.28456744824856628, -23.36843029042086428 ) ) ;
#28167=LINE ( 'NONE', #13695, #11255 ) ;
#28259=CYLINDRICAL_SURFACE ( 'NONE', #21482, 4.440000000000003055 ) ;
#28359=CARTESIAN_POINT ( 'NONE',  ( 11.20000000009999930, -32.00000000000000000, -25.51324865394999719 ) ) ;
#28376=ADVANCED_FACE ( 'NONE', ( #12129 ), #7764, .T. ) ;
#28410=SURFACE_STYLE_USAGE ( .BOTH. , #30770 ) ;
#28450=CARTESIAN_POINT ( 'NONE',  ( 14.81448010921228509, -28.73192765248866110, -23.62653622451373892 ) ) ;
#28477=CARTESIAN_POINT ( 'NONE',  ( 14.40197535836999876, -26.99999999999984368, -34.17350269180000311 ) ) ;
#28529=LINE ( 'NONE', #16258, #1354 ) ;
#28564=DIRECTION ( 'NONE',  ( 1.000000000000000000, 0.000000000000000000, 0.000000000000000000 ) ) ;
#28603=AXIS2_PLACEMENT_3D ( 'NONE', #24175, #5290, #10165 ) ;
#28640=VERTEX_POINT ( 'NONE', #10167 ) ;
#28676=EDGE_LOOP ( 'NONE', ( #163, #8989, #25148, #23282 ) ) ;
#28808=CARTESIAN_POINT ( 'NONE',  ( 14.74592307778630484, -25.66596092470346591, -23.39674041003665650 ) ) ;
#28818=ORIENTED_EDGE ( 'NONE', *, *, #7956, .T. ) ;
#28832=DIRECTION ( 'NONE',  ( 1.000000000000000000, 0.000000000000000000, 0.000000000000000000 ) ) ;
#28834=CARTESIAN_POINT ( 'NONE',  ( -20.22682926819999949, -26.99999999999973355, -28.39999999990017798 ) ) ;
#28855=( GEOMETRIC_REPRESENTATION_CONTEXT ( 3 ) GLOBAL_UNCERTAINTY_ASSIGNED_CONTEXT ( ( #19132 ) ) GLOBAL_UNIT_ASSIGNED_CONTEXT ( ( #22909, #13768, #30619 ) ) REPRESENTATION_CONTEXT ( 'NONE', 'WORKASPACE' ) );
#29016=ADVANCED_FACE ( 'NONE', ( #6638 ), #15240, .T. ) ;
#29020=AXIS2_PLACEMENT_3D ( 'NONE', #4388, #11624, #13357 ) ;
#29044=DIRECTION ( 'NONE',  ( 0.000000000000000000, 0.8660254037843289066, -0.5000000000001899592 ) ) ;
#29124=CARTESIAN_POINT ( 'NONE',  ( 14.40197535836999876, -27.00000000000014566, -22.62649730800000114 ) ) ;
#29136=ORIENTED_EDGE ( 'NONE', *, *, #21926, .F. ) ;
#29145=EDGE_CURVE ( 'NONE', #1536, #12797, #13518, .T. ) ;
#29179=UNCERTAINTY_MEASURE_WITH_UNIT (LENGTH_MEASURE( 1.000000000000000082E-05 ), #4494, 'distance_accuracy_value', 'NONE');
#29184=CARTESIAN_POINT ( 'NONE',  ( 14.63279312439391155, -31.99961502282818415, -26.42651388579572114 ) ) ;
#29203=DIRECTION ( 'NONE',  ( 1.000000000000000000, 0.000000000000000000, 0.000000000000000000 ) ) ;
#29229=CARTESIAN_POINT ( 'NONE',  ( 14.85000000009999788, -27.00000000000000000, -28.39999999989999679 ) ) ;
#29278=EDGE_LOOP ( 'NONE', ( #30072, #11219, #29939, #19046 ) ) ;
#29324=AXIS2_PLACEMENT_3D ( 'NONE', #18959, #28564, #2298 ) ;
#29336=VERTEX_POINT ( 'NONE', #29589 ) ;
#29341=CARTESIAN_POINT ( 'NONE',  ( 14.73716614372071376, -31.99975091343083022, -26.99668318814331158 ) ) ;
#29345=ADVANCED_FACE ( 'NONE', ( #24877 ), #12231, .T. ) ;
#29353=FACE_OUTER_BOUND ( 'NONE', #22298, .T. ) ;
#29366=CIRCLE ( 'NONE', #1736, 4.997501249380000843 ) ;
#29369=CARTESIAN_POINT ( 'NONE',  ( 10.45000000009999930, -26.99999999999950617, -28.39999999990030588 ) ) ;
#29410=CARTESIAN_POINT ( 'NONE',  ( 11.20000000009999930, -27.00000000000000000, -34.17350269180000311 ) ) ;
#29500=CARTESIAN_POINT ( 'NONE',  ( 14.74203063447135165, -31.99976192563964972, -27.02823022071577341 ) ) ;
#29589=CARTESIAN_POINT ( 'NONE',  ( 11.20000000009999930, -31.44000000000000128, -28.39999999989999679 ) ) ;
#29633=CARTESIAN_POINT ( 'NONE',  ( -19.29999999990000248, -26.99999999999986144, -28.39999999990009272 ) ) ;
#29678=CARTESIAN_POINT ( 'NONE',  ( 14.80403571755166148, -23.72938950558570781, -32.28486879153918210 ) ) ;
#29686=EDGE_LOOP ( 'NONE', ( #7720, #686, #28818, #23404 ) ) ;
#29704=CARTESIAN_POINT ( 'NONE',  ( -4.299999999899999814, -27.00000000000000000, -28.39999999989999679 ) ) ;
#29739=EDGE_CURVE ( 'NONE', #1536, #11539, #15739, .T. ) ;
#29768=AXIS2_PLACEMENT_3D ( 'NONE', #27463, #25270, #13460 ) ;
#29803=PLANE ( 'NONE',  #4982 ) ;
#29832=ORIENTED_EDGE ( 'NONE', *, *, #1050, .T. ) ;
#29854=DIRECTION ( 'NONE',  ( 1.000000000000000000, 0.000000000000000000, 0.000000000000000000 ) ) ;
#29886=CIRCLE ( 'NONE', #27867, 1.926829268289999231 ) ;
#29939=ORIENTED_EDGE ( 'NONE', *, *, #10425, .T. ) ;
#29979=CARTESIAN_POINT ( 'NONE',  ( 14.84835410051307036, -24.88989065226013153, -32.95556094950757142 ) ) ;
#30017=VECTOR ( 'NONE', #27367, 1000.000000000000114 ) ;
#30055=ORIENTED_EDGE ( 'NONE', *, *, #3875, .F. ) ;
#30071=ADVANCED_FACE ( 'NONE', ( #26009 ), #4762, .T. ) ;
#30072=ORIENTED_EDGE ( 'NONE', *, *, #20474, .F. ) ;
#30106=DIRECTION ( 'NONE',  ( 1.075528555106586974E-13, 0.9622309798138365400, 0.2722343503059523884 ) ) ;
#30187=CARTESIAN_POINT ( 'NONE',  ( 14.75111860152108534, -30.63528571087327634, -24.72562157583271514 ) ) ;
#30232=CARTESIAN_POINT ( 'NONE',  ( 11.20000000009999930, -22.55999999999999872, -28.39999999989999679 ) ) ;
#30264=CARTESIAN_POINT ( 'NONE',  ( 14.40197535836999876, -22.00000000000000000, -25.51324865394999719 ) ) ;
#30317=DIRECTION ( 'NONE',  ( 1.000000000000000000, 0.000000000000000000, 0.000000000000000000 ) ) ;
#30336=CARTESIAN_POINT ( 'NONE',  ( 14.68395928812249807, -22.95674027903807257, -24.96087439630253968 ) ) ;
#30346=VECTOR ( 'NONE', #2974, 1000.000000000000000 ) ;
#30386=( GEOMETRIC_REPRESENTATION_CONTEXT ( 3 ) GLOBAL_UNCERTAINTY_ASSIGNED_CONTEXT ( ( #29179 ) ) GLOBAL_UNIT_ASSIGNED_CONTEXT ( ( #4494, #2136, #21329 ) ) REPRESENTATION_CONTEXT ( 'NONE', 'WORKASPACE' ) );
#30423=ORIENTED_EDGE ( 'NONE', *, *, #17874, .T. ) ;
#30435=ORIENTED_EDGE ( 'NONE', *, *, #3129, .T. ) ;
#30462=PRESENTATION_STYLE_ASSIGNMENT (( #20864 ) ) ;
#30492=DIRECTION ( 'NONE',  ( 1.000000000000000000, 0.000000000000000000, 0.000000000000000000 ) ) ;
#30513=ORIENTED_EDGE ( 'NONE', *, *, #7721, .F. ) ;
#30564=CARTESIAN_POINT ( 'NONE',  ( 14.40197535836999876, -26.99999999999984368, -34.17350269180000311 ) ) ;
#30619=( NAMED_UNIT ( * ) SI_UNIT ( $, .STERADIAN. ) SOLID_ANGLE_UNIT ( ) );
#30654=AXIS2_PLACEMENT_3D ( 'NONE', #29410, #21183, #9060 ) ;
#30707=CARTESIAN_POINT ( 'NONE',  ( 14.73807200698136910, -22.00000000000000711, -26.99929886424486014 ) ) ;
#30733=VERTEX_POINT ( 'NONE', #20666 ) ;
#30770=SURFACE_SIDE_STYLE ('',( #11576 ) ) ;
#30775=CYLINDRICAL_SURFACE ( 'NONE', #13935, 2.926829268290000119 ) ;
#30792=DIRECTION ( 'NONE',  ( 0.000000000000000000, 1.000000000000000000, 0.000000000000000000 ) ) ;
#30815=CARTESIAN_POINT ( 'NONE',  ( 14.72975346148849241, -28.24357319906857455, -23.34478253265713832 ) ) ;
#31057=DIRECTION ( 'NONE',  ( 0.000000000000000000, 1.000000000000000000, 0.000000000000000000 ) ) ;
#31092=CARTESIAN_POINT ( 'NONE',  ( 11.20000000009999930, -22.00000000000000000, -28.39999999955988841 ) ) ;
ENDSEC;
END-ISO-10303-21;
